ISO-10303-21;
HEADER;
/* Generated by software containing ST-Developer
 * from STEP Tools, Inc. (www.steptools.com) 
 */

FILE_DESCRIPTION(
/* description */ ('Spring compression tester'),
/* implementation_level */ '2;1');

FILE_NAME(
/* name */ 'M4x10 Cap Screw.step',
/* time_stamp */ '2026-10-28T03:24:11-07:00',
/* author */ (''),
/* organization */ (''),
/* preprocessor_version */ 'ST-DEVELOPER v20.2',
/* originating_system */ 'Autodesk Translation Framework v15.17.0.0',
/* authorisation */ '');

FILE_SCHEMA (('AUTOMOTIVE_DESIGN { 1 0 10303 214 3 1 1 }'));
ENDSEC;

DATA;
#10=MECHANICAL_DESIGN_GEOMETRIC_PRESENTATION_REPRESENTATION('',(#1153),#43521);
#933=ORIENTED_CLOSED_SHELL('',*,#18592,.F.);
#940=BREP_WITH_VOIDS('Body1',#18593,(#933));
#961=CONICAL_SURFACE('',#20295,0.325,0.785398163397448);
#962=CONICAL_SURFACE('',#20299,0.335,0.785398163397448);
#963=CONICAL_SURFACE('',#20303,0.21,0.463647609000806);
#1018=SHAPE_REPRESENTATION_RELATIONSHIP('SRR','None',#43832,#1078);
#1078=ADVANCED_BREP_SHAPE_REPRESENTATION('',(#940),#43492);
#1153=STYLED_ITEM('',(#44209),#940);
#1470=FACE_BOUND('',#3997,.T.);
#1933=PLANE('',#20283);
#1934=PLANE('',#20284);
#1935=PLANE('',#20285);
#1936=PLANE('',#20286);
#1937=PLANE('',#20287);
#1938=PLANE('',#20288);
#1939=PLANE('',#20289);
#1940=PLANE('',#20290);
#1941=PLANE('',#20291);
#1942=PLANE('',#20293);
#1943=PLANE('',#20301);
#2713=FACE_OUTER_BOUND('',#3983,.T.);
#2714=FACE_OUTER_BOUND('',#3984,.T.);
#2715=FACE_OUTER_BOUND('',#3985,.T.);
#2716=FACE_OUTER_BOUND('',#3986,.T.);
#2717=FACE_OUTER_BOUND('',#3987,.T.);
#2718=FACE_OUTER_BOUND('',#3988,.T.);
#2719=FACE_OUTER_BOUND('',#3989,.T.);
#2720=FACE_OUTER_BOUND('',#3990,.T.);
#2721=FACE_OUTER_BOUND('',#3991,.T.);
#2722=FACE_OUTER_BOUND('',#3992,.T.);
#2723=FACE_OUTER_BOUND('',#3993,.T.);
#2724=FACE_OUTER_BOUND('',#3994,.T.);
#2725=FACE_OUTER_BOUND('',#3995,.T.);
#2726=FACE_OUTER_BOUND('',#3996,.T.);
#2727=FACE_OUTER_BOUND('',#3998,.T.);
#2728=FACE_OUTER_BOUND('',#3999,.T.);
#3983=EDGE_LOOP('',(#14597,#14598,#14599,#14600));
#3984=EDGE_LOOP('',(#14601,#14602,#14603,#14604));
#3985=EDGE_LOOP('',(#14605,#14606,#14607,#14608));
#3986=EDGE_LOOP('',(#14609,#14610,#14611,#14612));
#3987=EDGE_LOOP('',(#14613,#14614,#14615,#14616));
#3988=EDGE_LOOP('',(#14617,#14618,#14619,#14620));
#3989=EDGE_LOOP('',(#14621,#14622,#14623,#14624,#14625,#14626));
#3990=EDGE_LOOP('',(#14627,#14628,#14629,#14630,#14631,#14632));
#3991=EDGE_LOOP('',(#14633));
#3992=EDGE_LOOP('',(#14634));
#3993=EDGE_LOOP('',(#14635,#14636,#14637,#14638));
#3994=EDGE_LOOP('',(#14639,#14640,#14641,#14642));
#3995=EDGE_LOOP('',(#14643,#14644,#14645,#14646));
#3996=EDGE_LOOP('',(#14647));
#3997=EDGE_LOOP('',(#14648));
#3998=EDGE_LOOP('',(#14649,#14650,#14651,#14652));
#3999=EDGE_LOOP('',(#14653,#14654,#14655,#14656));
#5357=LINE('',#29677,#6789);
#5358=LINE('',#29679,#6790);
#5359=LINE('',#29681,#6791);
#5360=LINE('',#29682,#6792);
#5361=LINE('',#29685,#6793);
#5362=LINE('',#29687,#6794);
#5363=LINE('',#29688,#6795);
#5364=LINE('',#29691,#6796);
#5365=LINE('',#29693,#6797);
#5366=LINE('',#29694,#6798);
#5367=LINE('',#29697,#6799);
#5368=LINE('',#29699,#6800);
#5369=LINE('',#29700,#6801);
#5370=LINE('',#29703,#6802);
#5371=LINE('',#29705,#6803);
#5372=LINE('',#29706,#6804);
#5373=LINE('',#29708,#6805);
#5374=LINE('',#29709,#6806);
#5375=LINE('',#29721,#6807);
#5376=LINE('',#29725,#6808);
#5377=LINE('',#29729,#6809);
#5378=LINE('',#29736,#6810);
#5379=LINE('',#29738,#6811);
#6789=VECTOR('',#23947,1.);
#6790=VECTOR('',#23948,1.);
#6791=VECTOR('',#23949,1.);
#6792=VECTOR('',#23950,1.);
#6793=VECTOR('',#23953,1.);
#6794=VECTOR('',#23954,1.);
#6795=VECTOR('',#23955,1.);
#6796=VECTOR('',#23958,1.);
#6797=VECTOR('',#23959,1.);
#6798=VECTOR('',#23960,1.);
#6799=VECTOR('',#23963,1.);
#6800=VECTOR('',#23964,1.);
#6801=VECTOR('',#23965,1.);
#6802=VECTOR('',#23968,1.);
#6803=VECTOR('',#23969,1.);
#6804=VECTOR('',#23970,1.);
#6805=VECTOR('',#23973,1.);
#6806=VECTOR('',#23974,1.);
#6807=VECTOR('',#23991,0.325);
#6808=VECTOR('',#23996,0.35);
#6809=VECTOR('',#24001,0.335);
#6810=VECTOR('',#24010,0.21);
#6811=VECTOR('',#24013,0.2);
#7877=CIRCLE('',#20292,0.1954);
#7878=CIRCLE('',#20294,0.3);
#7879=CIRCLE('',#20296,0.35);
#7880=CIRCLE('',#20298,0.35);
#7881=CIRCLE('',#20300,0.32);
#7882=CIRCLE('',#20302,0.22);
#7883=CIRCLE('',#20304,0.1954);
#8944=VERTEX_POINT('',#29675);
#8945=VERTEX_POINT('',#29676);
#8946=VERTEX_POINT('',#29678);
#8947=VERTEX_POINT('',#29680);
#8948=VERTEX_POINT('',#29684);
#8949=VERTEX_POINT('',#29686);
#8950=VERTEX_POINT('',#29690);
#8951=VERTEX_POINT('',#29692);
#8952=VERTEX_POINT('',#29696);
#8953=VERTEX_POINT('',#29698);
#8954=VERTEX_POINT('',#29702);
#8955=VERTEX_POINT('',#29704);
#8956=VERTEX_POINT('',#29713);
#8957=VERTEX_POINT('',#29716);
#8958=VERTEX_POINT('',#29719);
#8959=VERTEX_POINT('',#29723);
#8960=VERTEX_POINT('',#29727);
#8961=VERTEX_POINT('',#29731);
#8962=VERTEX_POINT('',#29734);
#10963=EDGE_CURVE('',#8944,#8945,#5357,.T.);
#10964=EDGE_CURVE('',#8945,#8946,#5358,.T.);
#10965=EDGE_CURVE('',#8946,#8947,#5359,.T.);
#10966=EDGE_CURVE('',#8944,#8947,#5360,.T.);
#10967=EDGE_CURVE('',#8945,#8948,#5361,.T.);
#10968=EDGE_CURVE('',#8948,#8949,#5362,.T.);
#10969=EDGE_CURVE('',#8949,#8946,#5363,.T.);
#10970=EDGE_CURVE('',#8948,#8950,#5364,.T.);
#10971=EDGE_CURVE('',#8950,#8951,#5365,.T.);
#10972=EDGE_CURVE('',#8951,#8949,#5366,.T.);
#10973=EDGE_CURVE('',#8950,#8952,#5367,.T.);
#10974=EDGE_CURVE('',#8952,#8953,#5368,.T.);
#10975=EDGE_CURVE('',#8953,#8951,#5369,.T.);
#10976=EDGE_CURVE('',#8952,#8954,#5370,.T.);
#10977=EDGE_CURVE('',#8954,#8955,#5371,.T.);
#10978=EDGE_CURVE('',#8955,#8953,#5372,.T.);
#10979=EDGE_CURVE('',#8954,#8944,#5373,.T.);
#10980=EDGE_CURVE('',#8947,#8955,#5374,.T.);
#10981=EDGE_CURVE('',#8956,#8956,#7877,.T.);
#10982=EDGE_CURVE('',#8957,#8957,#7878,.T.);
#10983=EDGE_CURVE('',#8958,#8958,#7879,.T.);
#10984=EDGE_CURVE('',#8958,#8957,#5375,.T.);
#10985=EDGE_CURVE('',#8959,#8959,#7880,.T.);
#10986=EDGE_CURVE('',#8959,#8958,#5376,.T.);
#10987=EDGE_CURVE('',#8960,#8960,#7881,.T.);
#10988=EDGE_CURVE('',#8960,#8959,#5377,.T.);
#10989=EDGE_CURVE('',#8961,#8961,#7882,.T.);
#10990=EDGE_CURVE('',#8962,#8962,#7883,.F.);
#10991=EDGE_CURVE('',#8962,#8961,#5378,.T.);
#10992=EDGE_CURVE('',#8956,#8962,#5379,.T.);
#14597=ORIENTED_EDGE('',*,*,#10963,.T.);
#14598=ORIENTED_EDGE('',*,*,#10964,.T.);
#14599=ORIENTED_EDGE('',*,*,#10965,.T.);
#14600=ORIENTED_EDGE('',*,*,#10966,.F.);
#14601=ORIENTED_EDGE('',*,*,#10967,.T.);
#14602=ORIENTED_EDGE('',*,*,#10968,.T.);
#14603=ORIENTED_EDGE('',*,*,#10969,.T.);
#14604=ORIENTED_EDGE('',*,*,#10964,.F.);
#14605=ORIENTED_EDGE('',*,*,#10970,.T.);
#14606=ORIENTED_EDGE('',*,*,#10971,.T.);
#14607=ORIENTED_EDGE('',*,*,#10972,.T.);
#14608=ORIENTED_EDGE('',*,*,#10968,.F.);
#14609=ORIENTED_EDGE('',*,*,#10973,.T.);
#14610=ORIENTED_EDGE('',*,*,#10974,.T.);
#14611=ORIENTED_EDGE('',*,*,#10975,.T.);
#14612=ORIENTED_EDGE('',*,*,#10971,.F.);
#14613=ORIENTED_EDGE('',*,*,#10976,.T.);
#14614=ORIENTED_EDGE('',*,*,#10977,.T.);
#14615=ORIENTED_EDGE('',*,*,#10978,.T.);
#14616=ORIENTED_EDGE('',*,*,#10974,.F.);
#14617=ORIENTED_EDGE('',*,*,#10979,.T.);
#14618=ORIENTED_EDGE('',*,*,#10966,.T.);
#14619=ORIENTED_EDGE('',*,*,#10980,.T.);
#14620=ORIENTED_EDGE('',*,*,#10977,.F.);
#14621=ORIENTED_EDGE('',*,*,#10979,.F.);
#14622=ORIENTED_EDGE('',*,*,#10976,.F.);
#14623=ORIENTED_EDGE('',*,*,#10973,.F.);
#14624=ORIENTED_EDGE('',*,*,#10970,.F.);
#14625=ORIENTED_EDGE('',*,*,#10967,.F.);
#14626=ORIENTED_EDGE('',*,*,#10963,.F.);
#14627=ORIENTED_EDGE('',*,*,#10980,.F.);
#14628=ORIENTED_EDGE('',*,*,#10965,.F.);
#14629=ORIENTED_EDGE('',*,*,#10969,.F.);
#14630=ORIENTED_EDGE('',*,*,#10972,.F.);
#14631=ORIENTED_EDGE('',*,*,#10975,.F.);
#14632=ORIENTED_EDGE('',*,*,#10978,.F.);
#14633=ORIENTED_EDGE('',*,*,#10981,.F.);
#14634=ORIENTED_EDGE('',*,*,#10982,.F.);
#14635=ORIENTED_EDGE('',*,*,#10983,.F.);
#14636=ORIENTED_EDGE('',*,*,#10984,.T.);
#14637=ORIENTED_EDGE('',*,*,#10982,.T.);
#14638=ORIENTED_EDGE('',*,*,#10984,.F.);
#14639=ORIENTED_EDGE('',*,*,#10985,.F.);
#14640=ORIENTED_EDGE('',*,*,#10986,.T.);
#14641=ORIENTED_EDGE('',*,*,#10983,.T.);
#14642=ORIENTED_EDGE('',*,*,#10986,.F.);
#14643=ORIENTED_EDGE('',*,*,#10987,.F.);
#14644=ORIENTED_EDGE('',*,*,#10988,.T.);
#14645=ORIENTED_EDGE('',*,*,#10985,.T.);
#14646=ORIENTED_EDGE('',*,*,#10988,.F.);
#14647=ORIENTED_EDGE('',*,*,#10987,.T.);
#14648=ORIENTED_EDGE('',*,*,#10989,.F.);
#14649=ORIENTED_EDGE('',*,*,#10990,.F.);
#14650=ORIENTED_EDGE('',*,*,#10991,.T.);
#14651=ORIENTED_EDGE('',*,*,#10989,.T.);
#14652=ORIENTED_EDGE('',*,*,#10991,.F.);
#14653=ORIENTED_EDGE('',*,*,#10981,.T.);
#14654=ORIENTED_EDGE('',*,*,#10992,.T.);
#14655=ORIENTED_EDGE('',*,*,#10990,.T.);
#14656=ORIENTED_EDGE('',*,*,#10992,.F.);
#17254=CYLINDRICAL_SURFACE('',#20297,0.35);
#17255=CYLINDRICAL_SURFACE('',#20305,0.1954);
#18037=ADVANCED_FACE('',(#2713),#1933,.F.);
#18038=ADVANCED_FACE('',(#2714),#1934,.F.);
#18039=ADVANCED_FACE('',(#2715),#1935,.F.);
#18040=ADVANCED_FACE('',(#2716),#1936,.F.);
#18041=ADVANCED_FACE('',(#2717),#1937,.F.);
#18042=ADVANCED_FACE('',(#2718),#1938,.F.);
#18043=ADVANCED_FACE('',(#2719),#1939,.F.);
#18044=ADVANCED_FACE('',(#2720),#1940,.F.);
#18045=ADVANCED_FACE('',(#2721),#1941,.F.);
#18046=ADVANCED_FACE('',(#2722),#1942,.T.);
#18047=ADVANCED_FACE('',(#2723),#961,.T.);
#18048=ADVANCED_FACE('',(#2724),#17254,.T.);
#18049=ADVANCED_FACE('',(#2725),#962,.T.);
#18050=ADVANCED_FACE('',(#2726,#1470),#1943,.T.);
#18051=ADVANCED_FACE('',(#2727),#963,.T.);
#18052=ADVANCED_FACE('',(#2728),#17255,.T.);
#18592=CLOSED_SHELL('',(#18037,#18038,#18039,#18040,#18041,#18042,#18043,
#18044));
#18593=CLOSED_SHELL('',(#18045,#18046,#18047,#18048,#18049,#18050,#18051,
#18052));
#20282=AXIS2_PLACEMENT_3D('',#29673,#23943,#23944);
#20283=AXIS2_PLACEMENT_3D('',#29674,#23945,#23946);
#20284=AXIS2_PLACEMENT_3D('',#29683,#23951,#23952);
#20285=AXIS2_PLACEMENT_3D('',#29689,#23956,#23957);
#20286=AXIS2_PLACEMENT_3D('',#29695,#23961,#23962);
#20287=AXIS2_PLACEMENT_3D('',#29701,#23966,#23967);
#20288=AXIS2_PLACEMENT_3D('',#29707,#23971,#23972);
#20289=AXIS2_PLACEMENT_3D('',#29710,#23975,#23976);
#20290=AXIS2_PLACEMENT_3D('',#29711,#23977,#23978);
#20291=AXIS2_PLACEMENT_3D('',#29712,#23979,#23980);
#20292=AXIS2_PLACEMENT_3D('',#29714,#23981,#23982);
#20293=AXIS2_PLACEMENT_3D('',#29715,#23983,#23984);
#20294=AXIS2_PLACEMENT_3D('',#29717,#23985,#23986);
#20295=AXIS2_PLACEMENT_3D('',#29718,#23987,#23988);
#20296=AXIS2_PLACEMENT_3D('',#29720,#23989,#23990);
#20297=AXIS2_PLACEMENT_3D('',#29722,#23992,#23993);
#20298=AXIS2_PLACEMENT_3D('',#29724,#23994,#23995);
#20299=AXIS2_PLACEMENT_3D('',#29726,#23997,#23998);
#20300=AXIS2_PLACEMENT_3D('',#29728,#23999,#24000);
#20301=AXIS2_PLACEMENT_3D('',#29730,#24002,#24003);
#20302=AXIS2_PLACEMENT_3D('',#29732,#24004,#24005);
#20303=AXIS2_PLACEMENT_3D('',#29733,#24006,#24007);
#20304=AXIS2_PLACEMENT_3D('',#29735,#24008,#24009);
#20305=AXIS2_PLACEMENT_3D('',#29737,#24011,#24012);
#23943=DIRECTION('axis',(0.,0.,1.));
#23944=DIRECTION('refdir',(1.,0.,0.));
#23945=DIRECTION('center_axis',(0.866025403784439,0.,-0.5));
#23946=DIRECTION('ref_axis',(0.5,0.,0.866025403784439));
#23947=DIRECTION('',(-0.5,0.,-0.866025403784439));
#23948=DIRECTION('',(0.,-1.,0.));
#23949=DIRECTION('',(0.5,0.,0.866025403784439));
#23950=DIRECTION('',(0.,-1.,0.));
#23951=DIRECTION('center_axis',(1.60246890531964E-16,0.,-1.));
#23952=DIRECTION('ref_axis',(1.,0.,1.60246890531964E-16));
#23953=DIRECTION('',(-1.,0.,-1.60246890531964E-16));
#23954=DIRECTION('',(0.,-1.,0.));
#23955=DIRECTION('',(1.,0.,1.60246890531964E-16));
#23956=DIRECTION('center_axis',(-0.866025403784439,0.,-0.5));
#23957=DIRECTION('ref_axis',(0.5,0.,-0.866025403784439));
#23958=DIRECTION('',(-0.5,0.,0.866025403784439));
#23959=DIRECTION('',(0.,-1.,0.));
#23960=DIRECTION('',(0.5,0.,-0.866025403784439));
#23961=DIRECTION('center_axis',(-0.866025403784439,0.,0.5));
#23962=DIRECTION('ref_axis',(-0.5,0.,-0.866025403784439));
#23963=DIRECTION('',(0.5,0.,0.866025403784439));
#23964=DIRECTION('',(0.,-1.,0.));
#23965=DIRECTION('',(-0.5,0.,-0.866025403784439));
#23966=DIRECTION('center_axis',(-1.60246890531964E-16,0.,1.));
#23967=DIRECTION('ref_axis',(-1.,0.,-1.60246890531964E-16));
#23968=DIRECTION('',(1.,0.,1.60246890531964E-16));
#23969=DIRECTION('',(0.,-1.,0.));
#23970=DIRECTION('',(-1.,0.,-1.60246890531964E-16));
#23971=DIRECTION('center_axis',(0.866025403784439,0.,0.5));
#23972=DIRECTION('ref_axis',(-0.5,0.,0.866025403784439));
#23973=DIRECTION('',(0.5,0.,-0.866025403784439));
#23974=DIRECTION('',(-0.5,0.,0.866025403784439));
#23975=DIRECTION('center_axis',(0.,1.,0.));
#23976=DIRECTION('ref_axis',(1.,0.,0.));
#23977=DIRECTION('center_axis',(0.,-1.,0.));
#23978=DIRECTION('ref_axis',(0.,0.,-1.));
#23979=DIRECTION('center_axis',(0.,1.,0.));
#23980=DIRECTION('ref_axis',(1.,0.,0.));
#23981=DIRECTION('center_axis',(0.,1.,0.));
#23982=DIRECTION('ref_axis',(1.,0.,0.));
#23983=DIRECTION('center_axis',(0.,1.,0.));
#23984=DIRECTION('ref_axis',(0.,0.,1.));
#23985=DIRECTION('center_axis',(0.,-1.,0.));
#23986=DIRECTION('ref_axis',(1.,0.,0.));
#23987=DIRECTION('center_axis',(0.,-1.,0.));
#23988=DIRECTION('ref_axis',(1.,0.,0.));
#23989=DIRECTION('center_axis',(0.,-1.,0.));
#23990=DIRECTION('ref_axis',(1.,0.,0.));
#23991=DIRECTION('',(0.707106781186547,0.707106781186548,8.65956056235493E-17));
#23992=DIRECTION('center_axis',(0.,-1.,0.));
#23993=DIRECTION('ref_axis',(1.,0.,0.));
#23994=DIRECTION('center_axis',(0.,-1.,0.));
#23995=DIRECTION('ref_axis',(1.,0.,0.));
#23996=DIRECTION('',(0.,1.,0.));
#23997=DIRECTION('center_axis',(0.,1.,0.));
#23998=DIRECTION('ref_axis',(1.,0.,0.));
#23999=DIRECTION('center_axis',(0.,-1.,0.));
#24000=DIRECTION('ref_axis',(1.,0.,0.));
#24001=DIRECTION('',(-0.707106781186547,0.707106781186548,-8.65956056235493E-17));
#24002=DIRECTION('center_axis',(0.,-1.,0.));
#24003=DIRECTION('ref_axis',(0.,0.,-1.));
#24004=DIRECTION('center_axis',(0.,-1.,0.));
#24005=DIRECTION('ref_axis',(1.,0.,0.));
#24006=DIRECTION('center_axis',(0.,1.,0.));
#24007=DIRECTION('ref_axis',(1.,0.,0.));
#24008=DIRECTION('center_axis',(0.,1.,0.));
#24009=DIRECTION('ref_axis',(1.,0.,0.));
#24010=DIRECTION('',(-0.447213595499958,0.894427190999916,-5.47678698264203E-17));
#24011=DIRECTION('center_axis',(0.,-1.,0.));
#24012=DIRECTION('ref_axis',(1.,0.,0.));
#24013=DIRECTION('',(0.,1.,0.));
#29673=CARTESIAN_POINT('',(0.,0.,0.));
#29674=CARTESIAN_POINT('Origin',(0.0866025403784439,-0.4,-0.15));
#29675=CARTESIAN_POINT('',(0.173205080756888,-0.4,0.));
#29676=CARTESIAN_POINT('',(0.0866025403784439,-0.4,-0.15));
#29677=CARTESIAN_POINT('',(0.173205080756888,-0.4,0.));
#29678=CARTESIAN_POINT('',(0.0866025403784439,-0.64,-0.15));
#29679=CARTESIAN_POINT('',(0.0866025403784439,-0.4,-0.15));
#29680=CARTESIAN_POINT('',(0.173205080756888,-0.64,0.));
#29681=CARTESIAN_POINT('',(0.173205080756888,-0.64,0.));
#29682=CARTESIAN_POINT('',(0.173205080756888,-0.4,0.));
#29683=CARTESIAN_POINT('Origin',(-0.0866025403784438,-0.4,-0.15));
#29684=CARTESIAN_POINT('',(-0.0866025403784438,-0.4,-0.15));
#29685=CARTESIAN_POINT('',(0.0866025403784439,-0.4,-0.15));
#29686=CARTESIAN_POINT('',(-0.0866025403784438,-0.64,-0.15));
#29687=CARTESIAN_POINT('',(-0.0866025403784438,-0.4,-0.15));
#29688=CARTESIAN_POINT('',(0.0866025403784439,-0.64,-0.15));
#29689=CARTESIAN_POINT('Origin',(-0.173205080756888,-0.4,-2.77555756156289E-17));
#29690=CARTESIAN_POINT('',(-0.173205080756888,-0.4,-2.12115047744981E-17));
#29691=CARTESIAN_POINT('',(-0.0866025403784438,-0.4,-0.15));
#29692=CARTESIAN_POINT('',(-0.173205080756888,-0.64,-2.77555756156289E-17));
#29693=CARTESIAN_POINT('',(-0.173205080756888,-0.4,-2.12115047744981E-17));
#29694=CARTESIAN_POINT('',(-0.0866025403784438,-0.64,-0.15));
#29695=CARTESIAN_POINT('Origin',(-0.0866025403784439,-0.4,0.15));
#29696=CARTESIAN_POINT('',(-0.0866025403784439,-0.4,0.15));
#29697=CARTESIAN_POINT('',(-0.173205080756888,-0.4,-2.12115047744981E-17));
#29698=CARTESIAN_POINT('',(-0.0866025403784439,-0.64,0.15));
#29699=CARTESIAN_POINT('',(-0.0866025403784439,-0.4,0.15));
#29700=CARTESIAN_POINT('',(-0.173205080756888,-0.64,-2.12115047744981E-17));
#29701=CARTESIAN_POINT('Origin',(0.0866025403784439,-0.4,0.15));
#29702=CARTESIAN_POINT('',(0.0866025403784439,-0.4,0.15));
#29703=CARTESIAN_POINT('',(-0.0866025403784439,-0.4,0.15));
#29704=CARTESIAN_POINT('',(0.0866025403784439,-0.64,0.15));
#29705=CARTESIAN_POINT('',(0.0866025403784439,-0.4,0.15));
#29706=CARTESIAN_POINT('',(-0.0866025403784439,-0.64,0.15));
#29707=CARTESIAN_POINT('Origin',(0.173205080756888,-0.4,0.));
#29708=CARTESIAN_POINT('',(0.0866025403784439,-0.4,0.15));
#29709=CARTESIAN_POINT('',(0.0866025403784439,-0.64,0.15));
#29710=CARTESIAN_POINT('Origin',(0.,-0.4,-2.77555756156289E-17));
#29711=CARTESIAN_POINT('Origin',(0.,-0.64,-2.77555756156289E-17));
#29712=CARTESIAN_POINT('Origin',(0.,-1.,0.));
#29713=CARTESIAN_POINT('',(-0.1954,-1.,2.39295984553393E-17));
#29714=CARTESIAN_POINT('Origin',(0.,-1.,0.));
#29715=CARTESIAN_POINT('Origin',(0.3,0.4,0.));
#29716=CARTESIAN_POINT('',(-0.3,0.4,-3.67394039744206E-17));
#29717=CARTESIAN_POINT('Origin',(0.,0.4,0.));
#29718=CARTESIAN_POINT('Origin',(0.,0.375,0.));
#29719=CARTESIAN_POINT('',(-0.35,0.35,-4.28626379701573E-17));
#29720=CARTESIAN_POINT('Origin',(0.,0.35,0.));
#29721=CARTESIAN_POINT('',(-0.325,0.375,-3.9801020972289E-17));
#29722=CARTESIAN_POINT('Origin',(0.,0.19,0.));
#29723=CARTESIAN_POINT('',(-0.35,0.03,-4.28626379701574E-17));
#29724=CARTESIAN_POINT('Origin',(0.,0.03,0.));
#29725=CARTESIAN_POINT('',(-0.35,0.19,-4.28626379701574E-17));
#29726=CARTESIAN_POINT('Origin',(0.,0.0149999999999999,0.));
#29727=CARTESIAN_POINT('',(-0.32,-3.29597460435593E-17,-3.91886975727153E-17));
#29728=CARTESIAN_POINT('Origin',(0.,0.,0.));
#29729=CARTESIAN_POINT('',(-0.335,0.0149999999999999,-4.10256677714363E-17));
#29730=CARTESIAN_POINT('Origin',(0.22,0.,0.));
#29731=CARTESIAN_POINT('',(-0.22,-6.93889390390723E-18,-2.69422295812418E-17));
#29732=CARTESIAN_POINT('Origin',(0.,0.,0.));
#29733=CARTESIAN_POINT('Origin',(0.,-0.02,0.));
#29734=CARTESIAN_POINT('',(-0.1954,-0.0492,2.39295984553393E-17));
#29735=CARTESIAN_POINT('Origin',(0.,-0.0492,0.));
#29736=CARTESIAN_POINT('',(-0.21,-0.02,-2.57175827820944E-17));
#29737=CARTESIAN_POINT('Origin',(0.,-0.8,0.));
#29738=CARTESIAN_POINT('',(-0.1954,-0.8,-2.39295984553393E-17));
#43424=UNCERTAINTY_MEASURE_WITH_UNIT(LENGTH_MEASURE(0.001),#43522,
'DISTANCE_ACCURACY_VALUE',
'Maximum model space distance between geometric entities at asserted c
onnectivities');
#43453=UNCERTAINTY_MEASURE_WITH_UNIT(LENGTH_MEASURE(0.001),#43522,
'DISTANCE_ACCURACY_VALUE',
'Maximum model space distance between geometric entities at asserted c
onnectivities');
#43492=(
GEOMETRIC_REPRESENTATION_CONTEXT(3)
GLOBAL_UNCERTAINTY_ASSIGNED_CONTEXT((#43424))
GLOBAL_UNIT_ASSIGNED_CONTEXT((#43522,#43524,#43525))
REPRESENTATION_CONTEXT('','3D')
);
#43521=(
GEOMETRIC_REPRESENTATION_CONTEXT(3)
GLOBAL_UNCERTAINTY_ASSIGNED_CONTEXT((#43453))
GLOBAL_UNIT_ASSIGNED_CONTEXT((#43522,#43524,#43525))
REPRESENTATION_CONTEXT('','3D')
);
#43522=(
LENGTH_UNIT()
NAMED_UNIT(*)
SI_UNIT(.CENTI.,.METRE.)
);
#43524=(
NAMED_UNIT(*)
PLANE_ANGLE_UNIT()
SI_UNIT($,.RADIAN.)
);
#43525=(
NAMED_UNIT(*)
SI_UNIT($,.STERADIAN.)
SOLID_ANGLE_UNIT()
);
#43564=SHAPE_DEFINITION_REPRESENTATION(#43641,#43832);
#43641=PRODUCT_DEFINITION_SHAPE('',$,#43900);
#43832=SHAPE_REPRESENTATION('',(#20282),#43492);
#43861=PRODUCT_DEFINITION_CONTEXT('part definition',#44064,'design');
#43900=PRODUCT_DEFINITION('M4x10 Cap Screw','M4x10 Cap Screw',#43967,#43861);
#43967=PRODUCT_DEFINITION_FORMATION('',$,#44104);
#44064=APPLICATION_CONTEXT(
'Core Data for Automotive Mechanical Design Process');
#44065=PRODUCT_CONTEXT('part definition',#44064,'mechanical');
#44104=PRODUCT('M4x10 Cap Screw','M4x10 Cap Screw','M4x10 Cap Screw',(#44065));
#44203=COLOUR_RGB('Black',0.12,0.14,0.17);
#44204=FILL_AREA_STYLE_COLOUR('',#44203);
#44205=FILL_AREA_STYLE('',(#44204));
#44206=SURFACE_STYLE_FILL_AREA(#44205);
#44207=SURFACE_SIDE_STYLE('',(#44206));
#44208=SURFACE_STYLE_USAGE(.BOTH.,#44207);
#44209=PRESENTATION_STYLE_ASSIGNMENT((#44208));
ENDSEC;
END-ISO-10303-21;
